ISO-10303-21;
HEADER;
/* Generated by software containing ST-Developer
 * from STEP Tools, Inc. (www.steptools.com) 
 */

FILE_DESCRIPTION(
/* description */ ('Bearing friction torque test rig'),
/* implementation_level */ '2;1');

FILE_NAME(
/* name */ 'Seals 2RS (1).step',
/* time_stamp */ '2026-10-28T03:24:04-07:00',
/* author */ (''),
/* organization */ (''),
/* preprocessor_version */ 'ST-DEVELOPER v20.2',
/* originating_system */ 'Autodesk Translation Framework v15.17.0.0',
/* authorisation */ '');

FILE_SCHEMA (('AUTOMOTIVE_DESIGN { 1 0 10303 214 3 1 1 }'));
ENDSEC;

DATA;
#10=MECHANICAL_DESIGN_GEOMETRIC_PRESENTATION_REPRESENTATION('',(#578,#579),#14822);
#486=SHAPE_REPRESENTATION_RELATIONSHIP('SRR','None',#15027,#525);
#525=ADVANCED_BREP_SHAPE_REPRESENTATION('',(#631,#632),#14807);
#578=STYLED_ITEM('',(#15284),#631);
#579=STYLED_ITEM('',(#15284),#632);
#631=MANIFOLD_SOLID_BREP('Body1',#7695);
#632=MANIFOLD_SOLID_BREP('Body2',#7696);
#828=FACE_BOUND('',#2057,.T.);
#829=FACE_BOUND('',#2060,.T.);
#830=FACE_BOUND('',#2063,.T.);
#831=FACE_BOUND('',#2066,.T.);
#1031=PLANE('',#8863);
#1032=PLANE('',#8868);
#1033=PLANE('',#8871);
#1034=PLANE('',#8876);
#1427=FACE_OUTER_BOUND('',#2056,.T.);
#1428=FACE_OUTER_BOUND('',#2058,.T.);
#1429=FACE_OUTER_BOUND('',#2059,.T.);
#1430=FACE_OUTER_BOUND('',#2061,.T.);
#1431=FACE_OUTER_BOUND('',#2062,.T.);
#1432=FACE_OUTER_BOUND('',#2064,.T.);
#1433=FACE_OUTER_BOUND('',#2065,.T.);
#1434=FACE_OUTER_BOUND('',#2067,.T.);
#2056=EDGE_LOOP('',(#6590));
#2057=EDGE_LOOP('',(#6591));
#2058=EDGE_LOOP('',(#6592,#6593,#6594,#6595));
#2059=EDGE_LOOP('',(#6596));
#2060=EDGE_LOOP('',(#6597));
#2061=EDGE_LOOP('',(#6598,#6599,#6600,#6601));
#2062=EDGE_LOOP('',(#6602));
#2063=EDGE_LOOP('',(#6603));
#2064=EDGE_LOOP('',(#6604,#6605,#6606,#6607));
#2065=EDGE_LOOP('',(#6608));
#2066=EDGE_LOOP('',(#6609));
#2067=EDGE_LOOP('',(#6610,#6611,#6612,#6613));
#2550=LINE('',#13879,#2994);
#2551=LINE('',#13884,#2995);
#2552=LINE('',#13893,#2996);
#2553=LINE('',#13898,#2997);
#2994=VECTOR('',#10949,1.70469);
#2995=VECTOR('',#10956,1.65031);
#2996=VECTOR('',#10967,1.70469);
#2997=VECTOR('',#10974,1.65031);
#3459=CIRCLE('',#8864,1.70469);
#3460=CIRCLE('',#8865,1.65031);
#3461=CIRCLE('',#8867,1.70469);
#3462=CIRCLE('',#8869,1.65031);
#3463=CIRCLE('',#8872,1.70469);
#3464=CIRCLE('',#8873,1.65031);
#3465=CIRCLE('',#8875,1.70469);
#3466=CIRCLE('',#8877,1.65031);
#4050=VERTEX_POINT('',#13872);
#4051=VERTEX_POINT('',#13874);
#4052=VERTEX_POINT('',#13877);
#4053=VERTEX_POINT('',#13881);
#4054=VERTEX_POINT('',#13886);
#4055=VERTEX_POINT('',#13888);
#4056=VERTEX_POINT('',#13891);
#4057=VERTEX_POINT('',#13895);
#4921=EDGE_CURVE('',#4050,#4050,#3459,.T.);
#4922=EDGE_CURVE('',#4051,#4051,#3460,.T.);
#4923=EDGE_CURVE('',#4052,#4052,#3461,.T.);
#4924=EDGE_CURVE('',#4052,#4050,#2550,.T.);
#4925=EDGE_CURVE('',#4053,#4053,#3462,.T.);
#4926=EDGE_CURVE('',#4053,#4051,#2551,.T.);
#4927=EDGE_CURVE('',#4054,#4054,#3463,.T.);
#4928=EDGE_CURVE('',#4055,#4055,#3464,.T.);
#4929=EDGE_CURVE('',#4056,#4056,#3465,.T.);
#4930=EDGE_CURVE('',#4056,#4054,#2552,.T.);
#4931=EDGE_CURVE('',#4057,#4057,#3466,.T.);
#4932=EDGE_CURVE('',#4057,#4055,#2553,.T.);
#6590=ORIENTED_EDGE('',*,*,#4921,.F.);
#6591=ORIENTED_EDGE('',*,*,#4922,.T.);
#6592=ORIENTED_EDGE('',*,*,#4923,.F.);
#6593=ORIENTED_EDGE('',*,*,#4924,.T.);
#6594=ORIENTED_EDGE('',*,*,#4921,.T.);
#6595=ORIENTED_EDGE('',*,*,#4924,.F.);
#6596=ORIENTED_EDGE('',*,*,#4923,.T.);
#6597=ORIENTED_EDGE('',*,*,#4925,.F.);
#6598=ORIENTED_EDGE('',*,*,#4925,.T.);
#6599=ORIENTED_EDGE('',*,*,#4926,.T.);
#6600=ORIENTED_EDGE('',*,*,#4922,.F.);
#6601=ORIENTED_EDGE('',*,*,#4926,.F.);
#6602=ORIENTED_EDGE('',*,*,#4927,.F.);
#6603=ORIENTED_EDGE('',*,*,#4928,.T.);
#6604=ORIENTED_EDGE('',*,*,#4929,.F.);
#6605=ORIENTED_EDGE('',*,*,#4930,.T.);
#6606=ORIENTED_EDGE('',*,*,#4927,.T.);
#6607=ORIENTED_EDGE('',*,*,#4930,.F.);
#6608=ORIENTED_EDGE('',*,*,#4929,.T.);
#6609=ORIENTED_EDGE('',*,*,#4931,.F.);
#6610=ORIENTED_EDGE('',*,*,#4931,.T.);
#6611=ORIENTED_EDGE('',*,*,#4932,.T.);
#6612=ORIENTED_EDGE('',*,*,#4928,.F.);
#6613=ORIENTED_EDGE('',*,*,#4932,.F.);
#7170=CYLINDRICAL_SURFACE('',#8866,1.70469);
#7171=CYLINDRICAL_SURFACE('',#8870,1.65031);
#7172=CYLINDRICAL_SURFACE('',#8874,1.70469);
#7173=CYLINDRICAL_SURFACE('',#8878,1.65031);
#7538=ADVANCED_FACE('',(#1427,#828),#1031,.T.);
#7539=ADVANCED_FACE('',(#1428),#7170,.T.);
#7540=ADVANCED_FACE('',(#1429,#829),#1032,.T.);
#7541=ADVANCED_FACE('',(#1430),#7171,.F.);
#7542=ADVANCED_FACE('',(#1431,#830),#1033,.T.);
#7543=ADVANCED_FACE('',(#1432),#7172,.T.);
#7544=ADVANCED_FACE('',(#1433,#831),#1034,.T.);
#7545=ADVANCED_FACE('',(#1434),#7173,.F.);
#7695=CLOSED_SHELL('',(#7538,#7539,#7540,#7541));
#7696=CLOSED_SHELL('',(#7542,#7543,#7544,#7545));
#8862=AXIS2_PLACEMENT_3D('',#13870,#10937,#10938);
#8863=AXIS2_PLACEMENT_3D('',#13871,#10939,#10940);
#8864=AXIS2_PLACEMENT_3D('',#13873,#10941,#10942);
#8865=AXIS2_PLACEMENT_3D('',#13875,#10943,#10944);
#8866=AXIS2_PLACEMENT_3D('',#13876,#10945,#10946);
#8867=AXIS2_PLACEMENT_3D('',#13878,#10947,#10948);
#8868=AXIS2_PLACEMENT_3D('',#13880,#10950,#10951);
#8869=AXIS2_PLACEMENT_3D('',#13882,#10952,#10953);
#8870=AXIS2_PLACEMENT_3D('',#13883,#10954,#10955);
#8871=AXIS2_PLACEMENT_3D('',#13885,#10957,#10958);
#8872=AXIS2_PLACEMENT_3D('',#13887,#10959,#10960);
#8873=AXIS2_PLACEMENT_3D('',#13889,#10961,#10962);
#8874=AXIS2_PLACEMENT_3D('',#13890,#10963,#10964);
#8875=AXIS2_PLACEMENT_3D('',#13892,#10965,#10966);
#8876=AXIS2_PLACEMENT_3D('',#13894,#10968,#10969);
#8877=AXIS2_PLACEMENT_3D('',#13896,#10970,#10971);
#8878=AXIS2_PLACEMENT_3D('',#13897,#10972,#10973);
#10937=DIRECTION('axis',(0.,0.,1.));
#10938=DIRECTION('refdir',(1.,0.,0.));
#10939=DIRECTION('center_axis',(0.,1.,0.));
#10940=DIRECTION('ref_axis',(0.,0.,1.));
#10941=DIRECTION('center_axis',(0.,-1.,0.));
#10942=DIRECTION('ref_axis',(1.,0.,0.));
#10943=DIRECTION('center_axis',(0.,-1.,0.));
#10944=DIRECTION('ref_axis',(1.,0.,0.));
#10945=DIRECTION('center_axis',(0.,-1.,0.));
#10946=DIRECTION('ref_axis',(1.,0.,0.));
#10947=DIRECTION('center_axis',(0.,-1.,0.));
#10948=DIRECTION('ref_axis',(1.,0.,0.));
#10949=DIRECTION('',(0.,1.,0.));
#10950=DIRECTION('center_axis',(0.,-1.,0.));
#10951=DIRECTION('ref_axis',(0.,0.,-1.));
#10952=DIRECTION('center_axis',(0.,-1.,0.));
#10953=DIRECTION('ref_axis',(1.,0.,0.));
#10954=DIRECTION('center_axis',(0.,-1.,0.));
#10955=DIRECTION('ref_axis',(1.,0.,0.));
#10956=DIRECTION('',(0.,1.,0.));
#10957=DIRECTION('center_axis',(0.,1.,0.));
#10958=DIRECTION('ref_axis',(0.,0.,1.));
#10959=DIRECTION('center_axis',(0.,-1.,0.));
#10960=DIRECTION('ref_axis',(1.,0.,0.));
#10961=DIRECTION('center_axis',(0.,-1.,0.));
#10962=DIRECTION('ref_axis',(1.,0.,0.));
#10963=DIRECTION('center_axis',(0.,-1.,0.));
#10964=DIRECTION('ref_axis',(1.,0.,0.));
#10965=DIRECTION('center_axis',(0.,-1.,0.));
#10966=DIRECTION('ref_axis',(1.,0.,0.));
#10967=DIRECTION('',(0.,1.,0.));
#10968=DIRECTION('center_axis',(0.,-1.,0.));
#10969=DIRECTION('ref_axis',(0.,0.,-1.));
#10970=DIRECTION('center_axis',(0.,-1.,0.));
#10971=DIRECTION('ref_axis',(1.,0.,0.));
#10972=DIRECTION('center_axis',(0.,-1.,0.));
#10973=DIRECTION('ref_axis',(1.,0.,0.));
#10974=DIRECTION('',(0.,1.,0.));
#13870=CARTESIAN_POINT('',(0.,0.,0.));
#13871=CARTESIAN_POINT('Origin',(1.70469,0.695,0.));
#13872=CARTESIAN_POINT('',(-1.70469,0.695,-2.0876431520385E-16));
#13873=CARTESIAN_POINT('Origin',(0.,0.695,0.));
#13874=CARTESIAN_POINT('',(-1.65031,0.695,-2.02104685910087E-16));
#13875=CARTESIAN_POINT('Origin',(0.,0.695,0.));
#13876=CARTESIAN_POINT('Origin',(0.,0.6575,0.));
#13877=CARTESIAN_POINT('',(-1.70469,0.62,-2.0876431520385E-16));
#13878=CARTESIAN_POINT('Origin',(0.,0.62,0.));
#13879=CARTESIAN_POINT('',(-1.70469,0.6575,-2.0876431520385E-16));
#13880=CARTESIAN_POINT('Origin',(1.65031,0.62,0.));
#13881=CARTESIAN_POINT('',(-1.65031,0.62,-2.02104685910087E-16));
#13882=CARTESIAN_POINT('Origin',(0.,0.62,0.));
#13883=CARTESIAN_POINT('Origin',(0.,0.6575,0.));
#13884=CARTESIAN_POINT('',(-1.65031,0.6575,-2.02104685910087E-16));
#13885=CARTESIAN_POINT('Origin',(1.70469,-0.62,0.));
#13886=CARTESIAN_POINT('',(-1.70469,-0.62,-2.0876431520385E-16));
#13887=CARTESIAN_POINT('Origin',(0.,-0.62,0.));
#13888=CARTESIAN_POINT('',(-1.65031,-0.62,-2.02104685910087E-16));
#13889=CARTESIAN_POINT('Origin',(0.,-0.62,0.));
#13890=CARTESIAN_POINT('Origin',(0.,-0.6575,0.));
#13891=CARTESIAN_POINT('',(-1.70469,-0.695,-2.0876431520385E-16));
#13892=CARTESIAN_POINT('Origin',(0.,-0.695,0.));
#13893=CARTESIAN_POINT('',(-1.70469,-0.6575,-2.0876431520385E-16));
#13894=CARTESIAN_POINT('Origin',(1.65031,-0.695,0.));
#13895=CARTESIAN_POINT('',(-1.65031,-0.695,-2.02104685910087E-16));
#13896=CARTESIAN_POINT('Origin',(0.,-0.695,0.));
#13897=CARTESIAN_POINT('Origin',(0.,-0.6575,0.));
#13898=CARTESIAN_POINT('',(-1.65031,-0.6575,-2.02104685910087E-16));
#14762=UNCERTAINTY_MEASURE_WITH_UNIT(LENGTH_MEASURE(0.001),#14823,
'DISTANCE_ACCURACY_VALUE',
'Maximum model space distance between geometric entities at asserted c
onnectivities');
#14777=UNCERTAINTY_MEASURE_WITH_UNIT(LENGTH_MEASURE(0.001),#14823,
'DISTANCE_ACCURACY_VALUE',
'Maximum model space distance between geometric entities at asserted c
onnectivities');
#14807=(
GEOMETRIC_REPRESENTATION_CONTEXT(3)
GLOBAL_UNCERTAINTY_ASSIGNED_CONTEXT((#14762))
GLOBAL_UNIT_ASSIGNED_CONTEXT((#14823,#14825,#14826))
REPRESENTATION_CONTEXT('','3D')
);
#14822=(
GEOMETRIC_REPRESENTATION_CONTEXT(3)
GLOBAL_UNCERTAINTY_ASSIGNED_CONTEXT((#14777))
GLOBAL_UNIT_ASSIGNED_CONTEXT((#14823,#14825,#14826))
REPRESENTATION_CONTEXT('','3D')
);
#14823=(
LENGTH_UNIT()
NAMED_UNIT(*)
SI_UNIT(.CENTI.,.METRE.)
);
#14825=(
NAMED_UNIT(*)
PLANE_ANGLE_UNIT()
SI_UNIT($,.RADIAN.)
);
#14826=(
NAMED_UNIT(*)
SI_UNIT($,.STERADIAN.)
SOLID_ANGLE_UNIT()
);
#14856=SHAPE_DEFINITION_REPRESENTATION(#14905,#15027);
#14905=PRODUCT_DEFINITION_SHAPE('',$,#15072);
#15027=SHAPE_REPRESENTATION('',(#8862),#14807);
#15042=PRODUCT_DEFINITION_CONTEXT('part definition',#15176,'design');
#15072=PRODUCT_DEFINITION('Seals 2RS (1)','Seals 2RS (1)',#15116,#15042);
#15116=PRODUCT_DEFINITION_FORMATION('',$,#15207);
#15176=APPLICATION_CONTEXT(
'Core Data for Automotive Mechanical Design Process');
#15177=PRODUCT_CONTEXT('part definition',#15176,'mechanical');
#15207=PRODUCT('Seals 2RS (1)','Seals 2RS (1)','Seals 2RS (1)',(#15177));
#15278=COLOUR_RGB('Grey',0.48,0.52,0.57);
#15279=FILL_AREA_STYLE_COLOUR('',#15278);
#15280=FILL_AREA_STYLE('',(#15279));
#15281=SURFACE_STYLE_FILL_AREA(#15280);
#15282=SURFACE_SIDE_STYLE('',(#15281));
#15283=SURFACE_STYLE_USAGE(.BOTH.,#15282);
#15284=PRESENTATION_STYLE_ASSIGNMENT((#15283));
ENDSEC;
END-ISO-10303-21;
